ISO-10303-21;
HEADER;
/* Generated by software containing ST-Developer
 * from STEP Tools, Inc. (www.steptools.com) 
 */

FILE_DESCRIPTION(
/* description */ (''),
/* implementation_level */ '2;1');

FILE_NAME(
/* name */ 'Ball_02.step',
/* time_stamp */ '2026-10-04T23:23:09-07:00',
/* author */ (''),
/* organization */ (''),
/* preprocessor_version */ 'ST-DEVELOPER v20.2',
/* originating_system */ 'Autodesk Translation Framework v15.15.0.0',
/* authorisation */ '');

FILE_SCHEMA (('AUTOMOTIVE_DESIGN { 1 0 10303 214 3 1 1 }'));
ENDSEC;

DATA;
#10=MECHANICAL_DESIGN_GEOMETRIC_PRESENTATION_REPRESENTATION('',(#73),#2676);
#47=SPHERICAL_SURFACE('',#1709,1.);
#54=SHAPE_REPRESENTATION_RELATIONSHIP('SRR','None',#2713,#62);
#62=ADVANCED_BREP_SHAPE_REPRESENTATION('',(#84),#2673);
#73=STYLED_ITEM('',(#2757),#84);
#84=MANIFOLD_SOLID_BREP('Body1',#1484);
#253=FACE_OUTER_BOUND('',#371,.T.);
#371=EDGE_LOOP('',(#1216,#1217));
#689=CIRCLE('',#1710,1.);
#771=VERTEX_POINT('',#2498);
#772=VERTEX_POINT('',#2499);
#926=EDGE_CURVE('',#771,#772,#689,.T.);
#1216=ORIENTED_EDGE('',*,*,#926,.T.);
#1217=ORIENTED_EDGE('',*,*,#926,.F.);
#1444=ADVANCED_FACE('',(#253),#47,.T.);
#1484=CLOSED_SHELL('',(#1444));
#1708=AXIS2_PLACEMENT_3D('',#2496,#2075,#2076);
#1709=AXIS2_PLACEMENT_3D('',#2497,#2077,#2078);
#1710=AXIS2_PLACEMENT_3D('',#2500,#2079,#2080);
#2075=DIRECTION('axis',(0.,0.,1.));
#2076=DIRECTION('refdir',(1.,0.,0.));
#2077=DIRECTION('center_axis',(0.,0.,1.));
#2078=DIRECTION('ref_axis',(1.,0.,0.));
#2079=DIRECTION('center_axis',(0.,-1.,0.));
#2080=DIRECTION('ref_axis',(-1.,0.,0.));
#2496=CARTESIAN_POINT('',(0.,0.,0.));
#2497=CARTESIAN_POINT('Origin',(8.,-7.5,4.));
#2498=CARTESIAN_POINT('',(8.,-7.5,5.));
#2499=CARTESIAN_POINT('',(8.,-7.5,3.));
#2500=CARTESIAN_POINT('Origin',(8.,-7.5,4.));
#2663=UNCERTAINTY_MEASURE_WITH_UNIT(LENGTH_MEASURE(0.01),#2677,
'DISTANCE_ACCURACY_VALUE',
'Maximum model space distance between geometric entities at asserted c
onnectivities');
#2666=UNCERTAINTY_MEASURE_WITH_UNIT(LENGTH_MEASURE(0.01),#2677,
'DISTANCE_ACCURACY_VALUE',
'Maximum model space distance between geometric entities at asserted c
onnectivities');
#2673=(
GEOMETRIC_REPRESENTATION_CONTEXT(3)
GLOBAL_UNCERTAINTY_ASSIGNED_CONTEXT((#2663))
GLOBAL_UNIT_ASSIGNED_CONTEXT((#2677,#2679,#2680))
REPRESENTATION_CONTEXT('','3D')
);
#2676=(
GEOMETRIC_REPRESENTATION_CONTEXT(3)
GLOBAL_UNCERTAINTY_ASSIGNED_CONTEXT((#2666))
GLOBAL_UNIT_ASSIGNED_CONTEXT((#2677,#2679,#2680))
REPRESENTATION_CONTEXT('','3D')
);
#2677=(
LENGTH_UNIT()
NAMED_UNIT(*)
SI_UNIT(.MILLI.,.METRE.)
);
#2679=(
NAMED_UNIT(*)
PLANE_ANGLE_UNIT()
SI_UNIT($,.RADIAN.)
);
#2680=(
NAMED_UNIT(*)
SI_UNIT($,.STERADIAN.)
SOLID_ANGLE_UNIT()
);
#2687=SHAPE_DEFINITION_REPRESENTATION(#2696,#2713);
#2696=PRODUCT_DEFINITION_SHAPE('',$,#2723);
#2713=SHAPE_REPRESENTATION('',(#1708),#2673);
#2716=PRODUCT_DEFINITION_CONTEXT('part definition',#2745,'design');
#2723=PRODUCT_DEFINITION('Ball_02','Ball_02',#2732,#2716);
#2732=PRODUCT_DEFINITION_FORMATION('',$,#2753);
#2745=APPLICATION_CONTEXT(
'Core Data for Automotive Mechanical Design Process');
#2746=PRODUCT_CONTEXT('part definition',#2745,'mechanical');
#2753=PRODUCT('Ball_02','Ball_02',$,(#2746));
#2757=PRESENTATION_STYLE_ASSIGNMENT((#2759));
#2759=SURFACE_STYLE_USAGE(.BOTH.,#2761);
#2761=SURFACE_SIDE_STYLE('',(#2763));
#2763=SURFACE_STYLE_FILL_AREA(#2765);
#2765=FILL_AREA_STYLE('Opaque(203,203,203)',(#2767));
#2767=FILL_AREA_STYLE_COLOUR('Opaque(203,203,203)',#2769);
#2769=COLOUR_RGB('Opaque(203,203,203)', 0.09019608, 0.27058824, 0.51372549);
ENDSEC;
END-ISO-10303-21;
